ISO-10303-21;
HEADER;
/* Generated by software containing ST-Developer
 * from STEP Tools, Inc. (www.steptools.com) 
 */

FILE_DESCRIPTION(
/* description */ ('PAT-001'),
/* implementation_level */ '2;1');

FILE_NAME(
/* name */ 'Hex Nut - M8.step',
/* time_stamp */ '2026-10-29T17:07:15-07:00',
/* author */ (''),
/* organization */ (''),
/* preprocessor_version */ 'ST-DEVELOPER v20.2',
/* originating_system */ 'Autodesk Translation Framework v15.17.0.0',
/* authorisation */ '');

FILE_SCHEMA (('AUTOMOTIVE_DESIGN { 1 0 10303 214 3 1 1 }'));
ENDSEC;

DATA;
#10=MECHANICAL_DESIGN_GEOMETRIC_PRESENTATION_REPRESENTATION('',(#400),#9622);
#17=(
BOUNDED_CURVE()
B_SPLINE_CURVE(2,(#9219,#9220,#9221),.UNSPECIFIED.,.F.,.F.)
B_SPLINE_CURVE_WITH_KNOTS((3,3),(0.14973948338295,0.97160236658079),
 .UNSPECIFIED.)
CURVE()
GEOMETRIC_REPRESENTATION_ITEM()
RATIONAL_B_SPLINE_CURVE((1.07140024848292,1.23714644374248,1.07140024848292))
REPRESENTATION_ITEM('')
);
#18=(
BOUNDED_CURVE()
B_SPLINE_CURVE(2,(#9223,#9224,#9225),.UNSPECIFIED.,.F.,.F.)
B_SPLINE_CURVE_WITH_KNOTS((3,3),(0.14973948338295,0.971602366580789),
 .UNSPECIFIED.)
CURVE()
GEOMETRIC_REPRESENTATION_ITEM()
RATIONAL_B_SPLINE_CURVE((1.07140024848292,1.23714644374248,1.07140024848292))
REPRESENTATION_ITEM('')
);
#19=(
BOUNDED_CURVE()
B_SPLINE_CURVE(2,(#9230,#9231,#9232),.UNSPECIFIED.,.F.,.F.)
B_SPLINE_CURVE_WITH_KNOTS((3,3),(0.14973948338295,0.97160236658079),
 .UNSPECIFIED.)
CURVE()
GEOMETRIC_REPRESENTATION_ITEM()
RATIONAL_B_SPLINE_CURVE((1.07140024848292,1.23714644374248,1.07140024848292))
REPRESENTATION_ITEM('')
);
#20=(
BOUNDED_CURVE()
B_SPLINE_CURVE(2,(#9234,#9235,#9236),.UNSPECIFIED.,.F.,.F.)
B_SPLINE_CURVE_WITH_KNOTS((3,3),(0.14973948338295,0.97160236658079),
 .UNSPECIFIED.)
CURVE()
GEOMETRIC_REPRESENTATION_ITEM()
RATIONAL_B_SPLINE_CURVE((1.07140024848292,1.23714644374248,1.07140024848292))
REPRESENTATION_ITEM('')
);
#21=(
BOUNDED_CURVE()
B_SPLINE_CURVE(2,(#9238,#9239,#9240),.UNSPECIFIED.,.F.,.F.)
B_SPLINE_CURVE_WITH_KNOTS((3,3),(0.14973948338295,0.971602366580789),
 .UNSPECIFIED.)
CURVE()
GEOMETRIC_REPRESENTATION_ITEM()
RATIONAL_B_SPLINE_CURVE((1.07140024848292,1.23714644374248,1.07140024848292))
REPRESENTATION_ITEM('')
);
#22=(
BOUNDED_CURVE()
B_SPLINE_CURVE(2,(#9241,#9242,#9243),.UNSPECIFIED.,.F.,.F.)
B_SPLINE_CURVE_WITH_KNOTS((3,3),(0.14973948338295,0.97160236658079),
 .UNSPECIFIED.)
CURVE()
GEOMETRIC_REPRESENTATION_ITEM()
RATIONAL_B_SPLINE_CURVE((1.07140024848292,1.23714644374248,1.07140024848292))
REPRESENTATION_ITEM('')
);
#23=(
BOUNDED_CURVE()
B_SPLINE_CURVE(2,(#9250,#9251,#9252),.UNSPECIFIED.,.F.,.F.)
B_SPLINE_CURVE_WITH_KNOTS((3,3),(0.14973948338295,0.97160236658079),
 .UNSPECIFIED.)
CURVE()
GEOMETRIC_REPRESENTATION_ITEM()
RATIONAL_B_SPLINE_CURVE((1.07140024848292,1.23714644374248,1.07140024848292))
REPRESENTATION_ITEM('')
);
#24=(
BOUNDED_CURVE()
B_SPLINE_CURVE(2,(#9254,#9255,#9256),.UNSPECIFIED.,.F.,.F.)
B_SPLINE_CURVE_WITH_KNOTS((3,3),(0.14973948338295,0.97160236658079),
 .UNSPECIFIED.)
CURVE()
GEOMETRIC_REPRESENTATION_ITEM()
RATIONAL_B_SPLINE_CURVE((1.07140024848292,1.23714644374248,1.07140024848292))
REPRESENTATION_ITEM('')
);
#25=(
BOUNDED_CURVE()
B_SPLINE_CURVE(2,(#9258,#9259,#9260),.UNSPECIFIED.,.F.,.F.)
B_SPLINE_CURVE_WITH_KNOTS((3,3),(0.14973948338295,0.971602366580789),
 .UNSPECIFIED.)
CURVE()
GEOMETRIC_REPRESENTATION_ITEM()
RATIONAL_B_SPLINE_CURVE((1.07140024848292,1.23714644374248,1.07140024848292))
REPRESENTATION_ITEM('')
);
#26=(
BOUNDED_CURVE()
B_SPLINE_CURVE(2,(#9262,#9263,#9264),.UNSPECIFIED.,.F.,.F.)
B_SPLINE_CURVE_WITH_KNOTS((3,3),(0.14973948338295,0.97160236658079),
 .UNSPECIFIED.)
CURVE()
GEOMETRIC_REPRESENTATION_ITEM()
RATIONAL_B_SPLINE_CURVE((1.07140024848292,1.23714644374248,1.07140024848292))
REPRESENTATION_ITEM('')
);
#27=(
BOUNDED_CURVE()
B_SPLINE_CURVE(2,(#9266,#9267,#9268),.UNSPECIFIED.,.F.,.F.)
B_SPLINE_CURVE_WITH_KNOTS((3,3),(0.14973948338295,0.97160236658079),
 .UNSPECIFIED.)
CURVE()
GEOMETRIC_REPRESENTATION_ITEM()
RATIONAL_B_SPLINE_CURVE((1.07140024848292,1.23714644374248,1.07140024848292))
REPRESENTATION_ITEM('')
);
#28=(
BOUNDED_CURVE()
B_SPLINE_CURVE(2,(#9269,#9270,#9271),.UNSPECIFIED.,.F.,.F.)
B_SPLINE_CURVE_WITH_KNOTS((3,3),(0.14973948338295,0.971602366580789),
 .UNSPECIFIED.)
CURVE()
GEOMETRIC_REPRESENTATION_ITEM()
RATIONAL_B_SPLINE_CURVE((1.07140024848292,1.23714644374248,1.07140024848292))
REPRESENTATION_ITEM('')
);
#315=CONICAL_SURFACE('',#5931,0.734027674973257,1.0471975511966);
#316=CONICAL_SURFACE('',#5933,0.734027674973257,1.0471975511966);
#342=SHAPE_REPRESENTATION_RELATIONSHIP('SRR','None',#9766,#367);
#367=ADVANCED_BREP_SHAPE_REPRESENTATION('',(#432),#9615);
#400=STYLED_ITEM('',(#9969),#432);
#432=MANIFOLD_SOLID_BREP('Body1',#5226);
#491=FACE_BOUND('',#1311,.T.);
#492=FACE_BOUND('',#1313,.T.);
#686=PLANE('',#5935);
#687=PLANE('',#5936);
#688=PLANE('',#5937);
#689=PLANE('',#5941);
#690=PLANE('',#5942);
#691=PLANE('',#5943);
#692=PLANE('',#5944);
#693=PLANE('',#5945);
#951=FACE_OUTER_BOUND('',#1301,.T.);
#952=FACE_OUTER_BOUND('',#1302,.T.);
#953=FACE_OUTER_BOUND('',#1303,.T.);
#954=FACE_OUTER_BOUND('',#1304,.T.);
#955=FACE_OUTER_BOUND('',#1305,.T.);
#956=FACE_OUTER_BOUND('',#1306,.T.);
#957=FACE_OUTER_BOUND('',#1307,.T.);
#958=FACE_OUTER_BOUND('',#1308,.T.);
#959=FACE_OUTER_BOUND('',#1309,.T.);
#960=FACE_OUTER_BOUND('',#1310,.T.);
#961=FACE_OUTER_BOUND('',#1312,.T.);
#1301=EDGE_LOOP('',(#4581,#4582,#4583,#4584,#4585,#4586,#4587,#4588,#4589));
#1302=EDGE_LOOP('',(#4590,#4591,#4592,#4593,#4594,#4595,#4596,#4597,#4598));
#1303=EDGE_LOOP('',(#4599,#4600,#4601,#4602));
#1304=EDGE_LOOP('',(#4603,#4604,#4605,#4606));
#1305=EDGE_LOOP('',(#4607,#4608,#4609,#4610));
#1306=EDGE_LOOP('',(#4611,#4612,#4613,#4614));
#1307=EDGE_LOOP('',(#4615,#4616,#4617,#4618));
#1308=EDGE_LOOP('',(#4619,#4620,#4621,#4622));
#1309=EDGE_LOOP('',(#4623,#4624,#4625,#4626));
#1310=EDGE_LOOP('',(#4627));
#1311=EDGE_LOOP('',(#4628));
#1312=EDGE_LOOP('',(#4629));
#1313=EDGE_LOOP('',(#4630));
#1748=LINE('',#9227,#2153);
#1749=LINE('',#9248,#2154);
#1750=LINE('',#9273,#2155);
#1751=LINE('',#9274,#2156);
#1752=LINE('',#9276,#2157);
#1753=LINE('',#9278,#2158);
#1754=LINE('',#9283,#2159);
#1755=LINE('',#9286,#2160);
#1756=LINE('',#9288,#2161);
#2153=VECTOR('',#7303,0.734027674973257);
#2154=VECTOR('',#7310,0.734027674973257);
#2155=VECTOR('',#7313,1.);
#2156=VECTOR('',#7314,1.);
#2157=VECTOR('',#7317,1.);
#2158=VECTOR('',#7320,1.);
#2159=VECTOR('',#7325,0.4);
#2160=VECTOR('',#7330,1.);
#2161=VECTOR('',#7333,1.);
#2364=CIRCLE('',#5932,0.6175);
#2365=CIRCLE('',#5934,0.6175);
#2366=CIRCLE('',#5939,0.338975);
#2367=CIRCLE('',#5940,0.338975);
#2782=VERTEX_POINT('',#9217);
#2783=VERTEX_POINT('',#9218);
#2784=VERTEX_POINT('',#9222);
#2785=VERTEX_POINT('',#9226);
#2786=VERTEX_POINT('',#9229);
#2787=VERTEX_POINT('',#9233);
#2788=VERTEX_POINT('',#9237);
#2789=VERTEX_POINT('',#9245);
#2790=VERTEX_POINT('',#9247);
#2791=VERTEX_POINT('',#9249);
#2792=VERTEX_POINT('',#9253);
#2793=VERTEX_POINT('',#9257);
#2794=VERTEX_POINT('',#9261);
#2795=VERTEX_POINT('',#9265);
#2796=VERTEX_POINT('',#9280);
#2797=VERTEX_POINT('',#9282);
#3394=EDGE_CURVE('',#2782,#2783,#17,.T.);
#3395=EDGE_CURVE('',#2784,#2782,#18,.T.);
#3396=EDGE_CURVE('',#2784,#2785,#1748,.T.);
#3397=EDGE_CURVE('',#2785,#2785,#2364,.T.);
#3398=EDGE_CURVE('',#2786,#2784,#19,.T.);
#3399=EDGE_CURVE('',#2787,#2786,#20,.T.);
#3400=EDGE_CURVE('',#2788,#2787,#21,.T.);
#3401=EDGE_CURVE('',#2783,#2788,#22,.T.);
#3402=EDGE_CURVE('',#2789,#2789,#2365,.T.);
#3403=EDGE_CURVE('',#2789,#2790,#1749,.T.);
#3404=EDGE_CURVE('',#2791,#2790,#23,.T.);
#3405=EDGE_CURVE('',#2792,#2791,#24,.T.);
#3406=EDGE_CURVE('',#2793,#2792,#25,.T.);
#3407=EDGE_CURVE('',#2794,#2793,#26,.T.);
#3408=EDGE_CURVE('',#2795,#2794,#27,.T.);
#3409=EDGE_CURVE('',#2790,#2795,#28,.T.);
#3410=EDGE_CURVE('',#2786,#2795,#1750,.T.);
#3411=EDGE_CURVE('',#2787,#2794,#1751,.T.);
#3412=EDGE_CURVE('',#2784,#2790,#1752,.T.);
#3413=EDGE_CURVE('',#2782,#2791,#1753,.T.);
#3414=EDGE_CURVE('',#2796,#2796,#2366,.F.);
#3415=EDGE_CURVE('',#2796,#2797,#1754,.T.);
#3416=EDGE_CURVE('',#2797,#2797,#2367,.F.);
#3417=EDGE_CURVE('',#2783,#2792,#1755,.T.);
#3418=EDGE_CURVE('',#2788,#2793,#1756,.T.);
#4581=ORIENTED_EDGE('',*,*,#3394,.F.);
#4582=ORIENTED_EDGE('',*,*,#3395,.F.);
#4583=ORIENTED_EDGE('',*,*,#3396,.T.);
#4584=ORIENTED_EDGE('',*,*,#3397,.F.);
#4585=ORIENTED_EDGE('',*,*,#3396,.F.);
#4586=ORIENTED_EDGE('',*,*,#3398,.F.);
#4587=ORIENTED_EDGE('',*,*,#3399,.F.);
#4588=ORIENTED_EDGE('',*,*,#3400,.F.);
#4589=ORIENTED_EDGE('',*,*,#3401,.F.);
#4590=ORIENTED_EDGE('',*,*,#3402,.F.);
#4591=ORIENTED_EDGE('',*,*,#3403,.T.);
#4592=ORIENTED_EDGE('',*,*,#3404,.F.);
#4593=ORIENTED_EDGE('',*,*,#3405,.F.);
#4594=ORIENTED_EDGE('',*,*,#3406,.F.);
#4595=ORIENTED_EDGE('',*,*,#3407,.F.);
#4596=ORIENTED_EDGE('',*,*,#3408,.F.);
#4597=ORIENTED_EDGE('',*,*,#3409,.F.);
#4598=ORIENTED_EDGE('',*,*,#3403,.F.);
#4599=ORIENTED_EDGE('',*,*,#3399,.T.);
#4600=ORIENTED_EDGE('',*,*,#3410,.T.);
#4601=ORIENTED_EDGE('',*,*,#3408,.T.);
#4602=ORIENTED_EDGE('',*,*,#3411,.F.);
#4603=ORIENTED_EDGE('',*,*,#3398,.T.);
#4604=ORIENTED_EDGE('',*,*,#3412,.T.);
#4605=ORIENTED_EDGE('',*,*,#3409,.T.);
#4606=ORIENTED_EDGE('',*,*,#3410,.F.);
#4607=ORIENTED_EDGE('',*,*,#3395,.T.);
#4608=ORIENTED_EDGE('',*,*,#3413,.T.);
#4609=ORIENTED_EDGE('',*,*,#3404,.T.);
#4610=ORIENTED_EDGE('',*,*,#3412,.F.);
#4611=ORIENTED_EDGE('',*,*,#3414,.F.);
#4612=ORIENTED_EDGE('',*,*,#3415,.T.);
#4613=ORIENTED_EDGE('',*,*,#3416,.T.);
#4614=ORIENTED_EDGE('',*,*,#3415,.F.);
#4615=ORIENTED_EDGE('',*,*,#3394,.T.);
#4616=ORIENTED_EDGE('',*,*,#3417,.T.);
#4617=ORIENTED_EDGE('',*,*,#3405,.T.);
#4618=ORIENTED_EDGE('',*,*,#3413,.F.);
#4619=ORIENTED_EDGE('',*,*,#3400,.T.);
#4620=ORIENTED_EDGE('',*,*,#3411,.T.);
#4621=ORIENTED_EDGE('',*,*,#3407,.T.);
#4622=ORIENTED_EDGE('',*,*,#3418,.F.);
#4623=ORIENTED_EDGE('',*,*,#3401,.T.);
#4624=ORIENTED_EDGE('',*,*,#3418,.T.);
#4625=ORIENTED_EDGE('',*,*,#3406,.T.);
#4626=ORIENTED_EDGE('',*,*,#3417,.F.);
#4627=ORIENTED_EDGE('',*,*,#3402,.T.);
#4628=ORIENTED_EDGE('',*,*,#3414,.T.);
#4629=ORIENTED_EDGE('',*,*,#3397,.T.);
#4630=ORIENTED_EDGE('',*,*,#3416,.F.);
#4877=CYLINDRICAL_SURFACE('',#5938,0.338975);
#5138=ADVANCED_FACE('',(#951),#315,.T.);
#5139=ADVANCED_FACE('',(#952),#316,.T.);
#5140=ADVANCED_FACE('',(#953),#686,.T.);
#5141=ADVANCED_FACE('',(#954),#687,.T.);
#5142=ADVANCED_FACE('',(#955),#688,.T.);
#5143=ADVANCED_FACE('',(#956),#4877,.F.);
#5144=ADVANCED_FACE('',(#957),#689,.T.);
#5145=ADVANCED_FACE('',(#958),#690,.T.);
#5146=ADVANCED_FACE('',(#959),#691,.T.);
#5147=ADVANCED_FACE('',(#960,#491),#692,.T.);
#5148=ADVANCED_FACE('',(#961,#492),#693,.F.);
#5226=CLOSED_SHELL('',(#5138,#5139,#5140,#5141,#5142,#5143,#5144,#5145,
#5146,#5147,#5148));
#5930=AXIS2_PLACEMENT_3D('',#9215,#7299,#7300);
#5931=AXIS2_PLACEMENT_3D('',#9216,#7301,#7302);
#5932=AXIS2_PLACEMENT_3D('',#9228,#7304,#7305);
#5933=AXIS2_PLACEMENT_3D('',#9244,#7306,#7307);
#5934=AXIS2_PLACEMENT_3D('',#9246,#7308,#7309);
#5935=AXIS2_PLACEMENT_3D('',#9272,#7311,#7312);
#5936=AXIS2_PLACEMENT_3D('',#9275,#7315,#7316);
#5937=AXIS2_PLACEMENT_3D('',#9277,#7318,#7319);
#5938=AXIS2_PLACEMENT_3D('',#9279,#7321,#7322);
#5939=AXIS2_PLACEMENT_3D('',#9281,#7323,#7324);
#5940=AXIS2_PLACEMENT_3D('',#9284,#7326,#7327);
#5941=AXIS2_PLACEMENT_3D('',#9285,#7328,#7329);
#5942=AXIS2_PLACEMENT_3D('',#9287,#7331,#7332);
#5943=AXIS2_PLACEMENT_3D('',#9289,#7334,#7335);
#5944=AXIS2_PLACEMENT_3D('',#9290,#7336,#7337);
#5945=AXIS2_PLACEMENT_3D('',#9291,#7338,#7339);
#7299=DIRECTION('axis',(0.,0.,1.));
#7300=DIRECTION('refdir',(1.,0.,0.));
#7301=DIRECTION('center_axis',(0.,1.,0.));
#7302=DIRECTION('ref_axis',(1.,0.,0.));
#7303=DIRECTION('',(0.866025403784439,-0.5,1.06057523872491E-16));
#7304=DIRECTION('center_axis',(0.,-1.,0.));
#7305=DIRECTION('ref_axis',(1.,0.,0.));
#7306=DIRECTION('center_axis',(0.,-1.,0.));
#7307=DIRECTION('ref_axis',(1.,0.,0.));
#7308=DIRECTION('center_axis',(0.,1.,0.));
#7309=DIRECTION('ref_axis',(1.,0.,0.));
#7310=DIRECTION('',(-0.866025403784439,-0.5,-1.06057523872491E-16));
#7311=DIRECTION('center_axis',(1.4792020664489E-16,0.,-1.));
#7312=DIRECTION('ref_axis',(-1.,0.,-1.4792020664489E-16));
#7313=DIRECTION('',(0.,1.,0.));
#7314=DIRECTION('',(0.,1.,0.));
#7315=DIRECTION('center_axis',(-0.866025403784439,0.,-0.5));
#7316=DIRECTION('ref_axis',(-0.5,0.,0.866025403784439));
#7317=DIRECTION('',(0.,1.,0.));
#7318=DIRECTION('center_axis',(-0.866025403784439,0.,0.5));
#7319=DIRECTION('ref_axis',(0.5,0.,0.866025403784439));
#7320=DIRECTION('',(0.,1.,0.));
#7321=DIRECTION('center_axis',(0.,1.,0.));
#7322=DIRECTION('ref_axis',(1.,0.,0.));
#7323=DIRECTION('center_axis',(0.,1.,0.));
#7324=DIRECTION('ref_axis',(1.,0.,0.));
#7325=DIRECTION('',(0.,-1.,0.));
#7326=DIRECTION('center_axis',(0.,1.,0.));
#7327=DIRECTION('ref_axis',(1.,0.,0.));
#7328=DIRECTION('center_axis',(-2.95840413289779E-16,0.,1.));
#7329=DIRECTION('ref_axis',(1.,0.,2.95840413289779E-16));
#7330=DIRECTION('',(0.,1.,0.));
#7331=DIRECTION('center_axis',(0.866025403784439,0.,-0.5));
#7332=DIRECTION('ref_axis',(-0.5,0.,-0.866025403784439));
#7333=DIRECTION('',(0.,1.,0.));
#7334=DIRECTION('center_axis',(0.866025403784439,0.,0.5));
#7335=DIRECTION('ref_axis',(0.5,0.,-0.866025403784439));
#7336=DIRECTION('center_axis',(0.,1.,0.));
#7337=DIRECTION('ref_axis',(1.,0.,0.));
#7338=DIRECTION('center_axis',(0.,1.,0.));
#7339=DIRECTION('ref_axis',(1.,0.,0.));
#9215=CARTESIAN_POINT('',(0.,0.,0.));
#9216=CARTESIAN_POINT('Origin',(0.,0.067277284513851,0.));
#9217=CARTESIAN_POINT('',(-0.375277674973257,0.0768195421087395,0.65));
#9218=CARTESIAN_POINT('',(0.375277674973257,0.0768195421087395,0.65));
#9219=CARTESIAN_POINT('Ctrl Pts',(-0.375277674973257,0.0768195421087395,
0.65));
#9220=CARTESIAN_POINT('Ctrl Pts',(1.66533453693773E-13,-0.0315137912242439,
0.65));
#9221=CARTESIAN_POINT('Ctrl Pts',(0.375277674973257,0.0768195421087394,
0.65));
#9222=CARTESIAN_POINT('',(-0.750555349946514,0.0768195421087394,-9.19165206894919E-17));
#9223=CARTESIAN_POINT('Ctrl Pts',(-0.750555349946514,0.0768195421087394,
-9.19165206894919E-17));
#9224=CARTESIAN_POINT('Ctrl Pts',(-0.562916512459802,-0.0315137912242434,
0.325000000000144));
#9225=CARTESIAN_POINT('Ctrl Pts',(-0.375277674973257,0.0768195421087395,
0.65));
#9226=CARTESIAN_POINT('',(-0.6175,-2.77555756156289E-17,-7.5621939847349E-17));
#9227=CARTESIAN_POINT('',(-0.734027674973257,0.067277284513851,-8.98924642641573E-17));
#9228=CARTESIAN_POINT('Origin',(0.,0.,0.));
#9229=CARTESIAN_POINT('',(-0.375277674973257,0.0768195421087395,-0.65));
#9230=CARTESIAN_POINT('Ctrl Pts',(-0.375277674973257,0.0768195421087395,
-0.65));
#9231=CARTESIAN_POINT('Ctrl Pts',(-0.562916512459968,-0.0315137912242437,
-0.324999999999856));
#9232=CARTESIAN_POINT('Ctrl Pts',(-0.750555349946514,0.0768195421087395,
-9.19165206894919E-17));
#9233=CARTESIAN_POINT('',(0.375277674973257,0.0768195421087395,-0.65));
#9234=CARTESIAN_POINT('Ctrl Pts',(0.375277674973257,0.0768195421087395,
-0.65));
#9235=CARTESIAN_POINT('Ctrl Pts',(-1.66144875635155E-13,-0.0315137912242437,
-0.65));
#9236=CARTESIAN_POINT('Ctrl Pts',(-0.375277674973257,0.0768195421087395,
-0.65));
#9237=CARTESIAN_POINT('',(0.750555349946514,0.0768195421087394,0.));
#9238=CARTESIAN_POINT('Ctrl Pts',(0.750555349946514,0.0768195421087394,
0.));
#9239=CARTESIAN_POINT('Ctrl Pts',(0.562916512459802,-0.0315137912242436,
-0.325000000000144));
#9240=CARTESIAN_POINT('Ctrl Pts',(0.375277674973257,0.0768195421087395,
-0.65));
#9241=CARTESIAN_POINT('Ctrl Pts',(0.375277674973257,0.0768195421087394,
0.65));
#9242=CARTESIAN_POINT('Ctrl Pts',(0.562916512459968,-0.0315137912242439,
0.324999999999856));
#9243=CARTESIAN_POINT('Ctrl Pts',(0.750555349946514,0.0768195421087394,
0.));
#9244=CARTESIAN_POINT('Origin',(0.,0.612722715486149,0.));
#9245=CARTESIAN_POINT('',(-0.6175,0.68,-7.5621939847349E-17));
#9246=CARTESIAN_POINT('Origin',(0.,0.68,0.));
#9247=CARTESIAN_POINT('',(-0.750555349946514,0.603180457891261,-9.19165206894919E-17));
#9248=CARTESIAN_POINT('',(-0.734027674973257,0.612722715486149,-8.98924642641573E-17));
#9249=CARTESIAN_POINT('',(-0.375277674973257,0.603180457891261,0.65));
#9250=CARTESIAN_POINT('Ctrl Pts',(-0.375277674973257,0.603180457891261,
0.65));
#9251=CARTESIAN_POINT('Ctrl Pts',(-0.562916512459968,0.711513791224243,
0.324999999999856));
#9252=CARTESIAN_POINT('Ctrl Pts',(-0.750555349946514,0.603180457891261,
-9.19165206894919E-17));
#9253=CARTESIAN_POINT('',(0.375277674973257,0.603180457891261,0.65));
#9254=CARTESIAN_POINT('Ctrl Pts',(0.375277674973257,0.603180457891261,0.65));
#9255=CARTESIAN_POINT('Ctrl Pts',(-1.66755498298699E-13,0.711513791224244,
0.65));
#9256=CARTESIAN_POINT('Ctrl Pts',(-0.375277674973257,0.603180457891261,
0.65));
#9257=CARTESIAN_POINT('',(0.750555349946514,0.603180457891261,0.));
#9258=CARTESIAN_POINT('Ctrl Pts',(0.750555349946514,0.603180457891261,0.));
#9259=CARTESIAN_POINT('Ctrl Pts',(0.562916512459802,0.711513791224244,0.325000000000144));
#9260=CARTESIAN_POINT('Ctrl Pts',(0.375277674973257,0.603180457891261,0.65));
#9261=CARTESIAN_POINT('',(0.375277674973257,0.603180457891261,-0.65));
#9262=CARTESIAN_POINT('Ctrl Pts',(0.375277674973257,0.603180457891261,-0.65));
#9263=CARTESIAN_POINT('Ctrl Pts',(0.562916512459969,0.711513791224244,-0.324999999999856));
#9264=CARTESIAN_POINT('Ctrl Pts',(0.750555349946514,0.603180457891261,0.));
#9265=CARTESIAN_POINT('',(-0.375277674973257,0.603180457891261,-0.65));
#9266=CARTESIAN_POINT('Ctrl Pts',(-0.375277674973257,0.603180457891261,
-0.65));
#9267=CARTESIAN_POINT('Ctrl Pts',(1.66422431391311E-13,0.711513791224244,
-0.65));
#9268=CARTESIAN_POINT('Ctrl Pts',(0.375277674973257,0.603180457891261,-0.65));
#9269=CARTESIAN_POINT('Ctrl Pts',(-0.750555349946514,0.603180457891261,
-9.19165206894919E-17));
#9270=CARTESIAN_POINT('Ctrl Pts',(-0.562916512459802,0.711513791224244,
-0.325000000000144));
#9271=CARTESIAN_POINT('Ctrl Pts',(-0.375277674973257,0.603180457891261,
-0.65));
#9272=CARTESIAN_POINT('Origin',(0.375277674973257,0.,-0.65));
#9273=CARTESIAN_POINT('',(-0.375277674973257,0.,-0.65));
#9274=CARTESIAN_POINT('',(0.375277674973257,0.,-0.65));
#9275=CARTESIAN_POINT('Origin',(-0.375277674973257,0.,-0.65));
#9276=CARTESIAN_POINT('',(-0.750555349946514,0.,-9.19165206894919E-17));
#9277=CARTESIAN_POINT('Origin',(-0.750555349946514,0.,-9.19165206894919E-17));
#9278=CARTESIAN_POINT('',(-0.375277674973257,0.,0.65));
#9279=CARTESIAN_POINT('Origin',(0.,0.,0.));
#9280=CARTESIAN_POINT('',(-0.338975,0.68,4.15124648740974E-17));
#9281=CARTESIAN_POINT('Origin',(0.,0.68,0.));
#9282=CARTESIAN_POINT('',(-0.338975,0.,4.15124648740974E-17));
#9283=CARTESIAN_POINT('',(-0.338975,0.,4.15124648740974E-17));
#9284=CARTESIAN_POINT('Origin',(0.,0.,0.));
#9285=CARTESIAN_POINT('Origin',(-0.375277674973257,0.,0.65));
#9286=CARTESIAN_POINT('',(0.375277674973257,0.,0.65));
#9287=CARTESIAN_POINT('Origin',(0.750555349946514,0.,0.));
#9288=CARTESIAN_POINT('',(0.750555349946514,0.,0.));
#9289=CARTESIAN_POINT('Origin',(0.375277674973257,0.,0.65));
#9290=CARTESIAN_POINT('Origin',(0.,0.68,-1.11022302462516E-16));
#9291=CARTESIAN_POINT('Origin',(0.,0.,-1.11022302462516E-16));
#9585=UNCERTAINTY_MEASURE_WITH_UNIT(LENGTH_MEASURE(0.001),#9623,
'DISTANCE_ACCURACY_VALUE',
'Maximum model space distance between geometric entities at asserted c
onnectivities');
#9592=UNCERTAINTY_MEASURE_WITH_UNIT(LENGTH_MEASURE(0.001),#9623,
'DISTANCE_ACCURACY_VALUE',
'Maximum model space distance between geometric entities at asserted c
onnectivities');
#9615=(
GEOMETRIC_REPRESENTATION_CONTEXT(3)
GLOBAL_UNCERTAINTY_ASSIGNED_CONTEXT((#9585))
GLOBAL_UNIT_ASSIGNED_CONTEXT((#9623,#9625,#9626))
REPRESENTATION_CONTEXT('','3D')
);
#9622=(
GEOMETRIC_REPRESENTATION_CONTEXT(3)
GLOBAL_UNCERTAINTY_ASSIGNED_CONTEXT((#9592))
GLOBAL_UNIT_ASSIGNED_CONTEXT((#9623,#9625,#9626))
REPRESENTATION_CONTEXT('','3D')
);
#9623=(
LENGTH_UNIT()
NAMED_UNIT(*)
SI_UNIT(.CENTI.,.METRE.)
);
#9625=(
NAMED_UNIT(*)
PLANE_ANGLE_UNIT()
SI_UNIT($,.RADIAN.)
);
#9626=(
NAMED_UNIT(*)
SI_UNIT($,.STERADIAN.)
SOLID_ANGLE_UNIT()
);
#9649=SHAPE_DEFINITION_REPRESENTATION(#9683,#9766);
#9683=PRODUCT_DEFINITION_SHAPE('',$,#9796);
#9766=SHAPE_REPRESENTATION('',(#5930),#9615);
#9773=PRODUCT_DEFINITION_CONTEXT('part definition',#9862,'design');
#9796=PRODUCT_DEFINITION('Hex Nut - M8','Hex Nut - M8',#9825,#9773);
#9825=PRODUCT_DEFINITION_FORMATION('',$,#9886);
#9862=APPLICATION_CONTEXT(
'Core Data for Automotive Mechanical Design Process');
#9863=PRODUCT_CONTEXT('part definition',#9862,'mechanical');
#9886=PRODUCT('Hex Nut - M8','Hex Nut - M8','Hex Nut - M8',(#9863));
#9963=COLOUR_RGB('Black',0.12,0.14,0.17);
#9964=FILL_AREA_STYLE_COLOUR('',#9963);
#9965=FILL_AREA_STYLE('',(#9964));
#9966=SURFACE_STYLE_FILL_AREA(#9965);
#9967=SURFACE_SIDE_STYLE('',(#9966));
#9968=SURFACE_STYLE_USAGE(.BOTH.,#9967);
#9969=PRESENTATION_STYLE_ASSIGNMENT((#9968));
ENDSEC;
END-ISO-10303-21;
